ISO-10303-21;
HEADER;
/* Generated by software containing ST-Developer
 * from STEP Tools, Inc. (www.steptools.com) 
 */

FILE_DESCRIPTION(
/* description */ ('Jaw-coupled motor to shaft test stand'),
/* implementation_level */ '2;1');

FILE_NAME(
/* name */ 'Bonded pad (1).step',
/* time_stamp */ '2026-10-27T10:46:06-07:00',
/* author */ (''),
/* organization */ (''),
/* preprocessor_version */ 'ST-DEVELOPER v20.2',
/* originating_system */ 'Autodesk Translation Framework v15.17.0.0',
/* authorisation */ '');

FILE_SCHEMA (('AUTOMOTIVE_DESIGN { 1 0 10303 214 3 1 1 }'));
ENDSEC;

DATA;
#10=MECHANICAL_DESIGN_GEOMETRIC_PRESENTATION_REPRESENTATION('',(#342),#19361);
#278=SHAPE_REPRESENTATION_RELATIONSHIP('SRR','None',#19492,#310);
#310=ADVANCED_BREP_SHAPE_REPRESENTATION('',(#375),#19328);
#342=STYLED_ITEM('',(#19760),#375);
#375=MANIFOLD_SOLID_BREP('Body1',#10986);
#528=PLANE('',#11408);
#529=PLANE('',#11409);
#530=PLANE('',#11410);
#531=PLANE('',#11411);
#532=PLANE('',#11412);
#533=PLANE('',#11413);
#1040=FACE_OUTER_BOUND('',#1672,.T.);
#1041=FACE_OUTER_BOUND('',#1673,.T.);
#1042=FACE_OUTER_BOUND('',#1674,.T.);
#1043=FACE_OUTER_BOUND('',#1675,.T.);
#1044=FACE_OUTER_BOUND('',#1676,.T.);
#1045=FACE_OUTER_BOUND('',#1677,.T.);
#1672=EDGE_LOOP('',(#7430,#7431,#7432,#7433));
#1673=EDGE_LOOP('',(#7434,#7435,#7436,#7437));
#1674=EDGE_LOOP('',(#7438,#7439,#7440,#7441));
#1675=EDGE_LOOP('',(#7442,#7443,#7444,#7445));
#1676=EDGE_LOOP('',(#7446,#7447,#7448,#7449));
#1677=EDGE_LOOP('',(#7450,#7451,#7452,#7453));
#2405=LINE('',#15523,#3558);
#2406=LINE('',#15525,#3559);
#2407=LINE('',#15527,#3560);
#2408=LINE('',#15528,#3561);
#2409=LINE('',#15531,#3562);
#2410=LINE('',#15533,#3563);
#2411=LINE('',#15534,#3564);
#2412=LINE('',#15537,#3565);
#2413=LINE('',#15539,#3566);
#2414=LINE('',#15540,#3567);
#2415=LINE('',#15542,#3568);
#2416=LINE('',#15543,#3569);
#3558=VECTOR('',#12442,1.);
#3559=VECTOR('',#12443,1.);
#3560=VECTOR('',#12444,1.);
#3561=VECTOR('',#12445,1.);
#3562=VECTOR('',#12448,1.);
#3563=VECTOR('',#12449,1.);
#3564=VECTOR('',#12450,1.);
#3565=VECTOR('',#12453,1.);
#3566=VECTOR('',#12454,1.);
#3567=VECTOR('',#12455,1.);
#3568=VECTOR('',#12458,1.);
#3569=VECTOR('',#12459,1.);
#4971=VERTEX_POINT('',#15521);
#4972=VERTEX_POINT('',#15522);
#4973=VERTEX_POINT('',#15524);
#4974=VERTEX_POINT('',#15526);
#4975=VERTEX_POINT('',#15530);
#4976=VERTEX_POINT('',#15532);
#4977=VERTEX_POINT('',#15536);
#4978=VERTEX_POINT('',#15538);
#5926=EDGE_CURVE('',#4971,#4972,#2405,.T.);
#5927=EDGE_CURVE('',#4972,#4973,#2406,.T.);
#5928=EDGE_CURVE('',#4974,#4973,#2407,.T.);
#5929=EDGE_CURVE('',#4971,#4974,#2408,.T.);
#5930=EDGE_CURVE('',#4975,#4971,#2409,.T.);
#5931=EDGE_CURVE('',#4976,#4974,#2410,.T.);
#5932=EDGE_CURVE('',#4975,#4976,#2411,.T.);
#5933=EDGE_CURVE('',#4977,#4975,#2412,.T.);
#5934=EDGE_CURVE('',#4978,#4976,#2413,.T.);
#5935=EDGE_CURVE('',#4977,#4978,#2414,.T.);
#5936=EDGE_CURVE('',#4972,#4977,#2415,.T.);
#5937=EDGE_CURVE('',#4973,#4978,#2416,.T.);
#7430=ORIENTED_EDGE('',*,*,#5926,.T.);
#7431=ORIENTED_EDGE('',*,*,#5927,.T.);
#7432=ORIENTED_EDGE('',*,*,#5928,.F.);
#7433=ORIENTED_EDGE('',*,*,#5929,.F.);
#7434=ORIENTED_EDGE('',*,*,#5930,.T.);
#7435=ORIENTED_EDGE('',*,*,#5929,.T.);
#7436=ORIENTED_EDGE('',*,*,#5931,.F.);
#7437=ORIENTED_EDGE('',*,*,#5932,.F.);
#7438=ORIENTED_EDGE('',*,*,#5933,.T.);
#7439=ORIENTED_EDGE('',*,*,#5932,.T.);
#7440=ORIENTED_EDGE('',*,*,#5934,.F.);
#7441=ORIENTED_EDGE('',*,*,#5935,.F.);
#7442=ORIENTED_EDGE('',*,*,#5936,.T.);
#7443=ORIENTED_EDGE('',*,*,#5935,.T.);
#7444=ORIENTED_EDGE('',*,*,#5937,.F.);
#7445=ORIENTED_EDGE('',*,*,#5927,.F.);
#7446=ORIENTED_EDGE('',*,*,#5937,.T.);
#7447=ORIENTED_EDGE('',*,*,#5934,.T.);
#7448=ORIENTED_EDGE('',*,*,#5931,.T.);
#7449=ORIENTED_EDGE('',*,*,#5928,.T.);
#7450=ORIENTED_EDGE('',*,*,#5936,.F.);
#7451=ORIENTED_EDGE('',*,*,#5926,.F.);
#7452=ORIENTED_EDGE('',*,*,#5930,.F.);
#7453=ORIENTED_EDGE('',*,*,#5933,.F.);
#10382=ADVANCED_FACE('',(#1040),#528,.T.);
#10383=ADVANCED_FACE('',(#1041),#529,.T.);
#10384=ADVANCED_FACE('',(#1042),#530,.T.);
#10385=ADVANCED_FACE('',(#1043),#531,.T.);
#10386=ADVANCED_FACE('',(#1044),#532,.T.);
#10387=ADVANCED_FACE('',(#1045),#533,.F.);
#10986=CLOSED_SHELL('',(#10382,#10383,#10384,#10385,#10386,#10387));
#11407=AXIS2_PLACEMENT_3D('',#15519,#12438,#12439);
#11408=AXIS2_PLACEMENT_3D('',#15520,#12440,#12441);
#11409=AXIS2_PLACEMENT_3D('',#15529,#12446,#12447);
#11410=AXIS2_PLACEMENT_3D('',#15535,#12451,#12452);
#11411=AXIS2_PLACEMENT_3D('',#15541,#12456,#12457);
#11412=AXIS2_PLACEMENT_3D('',#15544,#12460,#12461);
#11413=AXIS2_PLACEMENT_3D('',#15545,#12462,#12463);
#12438=DIRECTION('axis',(0.,0.,1.));
#12439=DIRECTION('refdir',(1.,0.,0.));
#12440=DIRECTION('center_axis',(0.,1.,0.));
#12441=DIRECTION('ref_axis',(-1.,0.,0.));
#12442=DIRECTION('',(-1.,0.,0.));
#12443=DIRECTION('',(0.,0.,1.));
#12444=DIRECTION('',(-1.,0.,0.));
#12445=DIRECTION('',(0.,0.,1.));
#12446=DIRECTION('center_axis',(1.,0.,0.));
#12447=DIRECTION('ref_axis',(0.,1.,0.));
#12448=DIRECTION('',(0.,1.,0.));
#12449=DIRECTION('',(0.,1.,0.));
#12450=DIRECTION('',(0.,0.,1.));
#12451=DIRECTION('center_axis',(0.,-1.,0.));
#12452=DIRECTION('ref_axis',(1.,0.,0.));
#12453=DIRECTION('',(1.,0.,0.));
#12454=DIRECTION('',(1.,0.,0.));
#12455=DIRECTION('',(0.,0.,1.));
#12456=DIRECTION('center_axis',(-1.,0.,0.));
#12457=DIRECTION('ref_axis',(0.,-1.,0.));
#12458=DIRECTION('',(0.,-1.,0.));
#12459=DIRECTION('',(0.,-1.,0.));
#12460=DIRECTION('center_axis',(0.,0.,1.));
#12461=DIRECTION('ref_axis',(1.,0.,0.));
#12462=DIRECTION('center_axis',(0.,0.,1.));
#12463=DIRECTION('ref_axis',(1.,0.,0.));
#15519=CARTESIAN_POINT('',(0.,0.,0.));
#15520=CARTESIAN_POINT('Origin',(7.,25.,-0.5));
#15521=CARTESIAN_POINT('',(7.,25.,-0.5));
#15522=CARTESIAN_POINT('',(-7.,25.,-0.5));
#15523=CARTESIAN_POINT('',(7.,25.,-0.5));
#15524=CARTESIAN_POINT('',(-7.,25.,0.));
#15525=CARTESIAN_POINT('',(-7.,25.,-0.5));
#15526=CARTESIAN_POINT('',(7.,25.,0.));
#15527=CARTESIAN_POINT('',(7.,25.,0.));
#15528=CARTESIAN_POINT('',(7.,25.,-0.5));
#15529=CARTESIAN_POINT('Origin',(7.,24.,-0.5));
#15530=CARTESIAN_POINT('',(7.,24.,-0.5));
#15531=CARTESIAN_POINT('',(7.,24.,-0.5));
#15532=CARTESIAN_POINT('',(7.,24.,0.));
#15533=CARTESIAN_POINT('',(7.,24.,0.));
#15534=CARTESIAN_POINT('',(7.,24.,-0.5));
#15535=CARTESIAN_POINT('Origin',(-7.,24.,-0.5));
#15536=CARTESIAN_POINT('',(-7.,24.,-0.5));
#15537=CARTESIAN_POINT('',(-7.,24.,-0.5));
#15538=CARTESIAN_POINT('',(-7.,24.,0.));
#15539=CARTESIAN_POINT('',(-7.,24.,0.));
#15540=CARTESIAN_POINT('',(-7.,24.,-0.5));
#15541=CARTESIAN_POINT('Origin',(-7.,25.,-0.5));
#15542=CARTESIAN_POINT('',(-7.,25.,-0.5));
#15543=CARTESIAN_POINT('',(-7.,25.,0.));
#15544=CARTESIAN_POINT('Origin',(0.,24.5,0.));
#15545=CARTESIAN_POINT('Origin',(0.,24.5,-0.5));
#19290=UNCERTAINTY_MEASURE_WITH_UNIT(LENGTH_MEASURE(0.001),#19362,
'DISTANCE_ACCURACY_VALUE',
'Maximum model space distance between geometric entities at asserted c
onnectivities');
#19323=UNCERTAINTY_MEASURE_WITH_UNIT(LENGTH_MEASURE(0.001),#19362,
'DISTANCE_ACCURACY_VALUE',
'Maximum model space distance between geometric entities at asserted c
onnectivities');
#19328=(
GEOMETRIC_REPRESENTATION_CONTEXT(3)
GLOBAL_UNCERTAINTY_ASSIGNED_CONTEXT((#19290))
GLOBAL_UNIT_ASSIGNED_CONTEXT((#19362,#19364,#19365))
REPRESENTATION_CONTEXT('','3D')
);
#19361=(
GEOMETRIC_REPRESENTATION_CONTEXT(3)
GLOBAL_UNCERTAINTY_ASSIGNED_CONTEXT((#19323))
GLOBAL_UNIT_ASSIGNED_CONTEXT((#19362,#19364,#19365))
REPRESENTATION_CONTEXT('','3D')
);
#19362=(
LENGTH_UNIT()
NAMED_UNIT(*)
SI_UNIT(.CENTI.,.METRE.)
);
#19364=(
NAMED_UNIT(*)
PLANE_ANGLE_UNIT()
SI_UNIT($,.RADIAN.)
);
#19365=(
NAMED_UNIT(*)
SI_UNIT($,.STERADIAN.)
SOLID_ANGLE_UNIT()
);
#19370=SHAPE_DEFINITION_REPRESENTATION(#19407,#19492);
#19407=PRODUCT_DEFINITION_SHAPE('',$,#19530);
#19492=SHAPE_REPRESENTATION('',(#11407),#19328);
#19525=PRODUCT_DEFINITION_CONTEXT('part definition',#19638,'design');
#19530=PRODUCT_DEFINITION('Bonded pad (1)','Bonded pad (1)',#19567,#19525);
#19567=PRODUCT_DEFINITION_FORMATION('',$,#19644);
#19638=APPLICATION_CONTEXT(
'Core Data for Automotive Mechanical Design Process');
#19639=PRODUCT_CONTEXT('part definition',#19638,'mechanical');
#19644=PRODUCT('Bonded pad (1)','Bonded pad (1)','Bonded pad (1)',(#19639));
#19754=COLOUR_RGB('Off White',0.89,0.88,0.83);
#19755=FILL_AREA_STYLE_COLOUR('',#19754);
#19756=FILL_AREA_STYLE('',(#19755));
#19757=SURFACE_STYLE_FILL_AREA(#19756);
#19758=SURFACE_SIDE_STYLE('',(#19757));
#19759=SURFACE_STYLE_USAGE(.BOTH.,#19758);
#19760=PRESENTATION_STYLE_ASSIGNMENT((#19759));
ENDSEC;
END-ISO-10303-21;
